ISO-10303-21;
HEADER;
/* Generated by software containing ST-Developer
 * from STEP Tools, Inc. (www.steptools.com) 
 */

FILE_DESCRIPTION(
/* description */ ('Bearing housing with oil seal and end cap'),
/* implementation_level */ '2;1');

FILE_NAME(
/* name */ 'Cap Screw - M4x16.step',
/* time_stamp */ '2026-10-28T03:23:10-07:00',
/* author */ (''),
/* organization */ (''),
/* preprocessor_version */ 'ST-DEVELOPER v20.2',
/* originating_system */ 'Autodesk Translation Framework v15.17.0.0',
/* authorisation */ '');

FILE_SCHEMA (('AUTOMOTIVE_DESIGN { 1 0 10303 214 3 1 1 }'));
ENDSEC;

DATA;
#10=MECHANICAL_DESIGN_GEOMETRIC_PRESENTATION_REPRESENTATION('',(#281),#7871);
#12=ORIENTED_CLOSED_SHELL('',*,#4109,.F.);
#14=BREP_WITH_VOIDS('Body1',#4108,(#12));
#209=CONICAL_SURFACE('',#4718,0.325,0.785398163397448);
#210=CONICAL_SURFACE('',#4722,0.335,0.785398163397448);
#211=CONICAL_SURFACE('',#4726,0.21,0.463647609000806);
#212=CONICAL_SURFACE('',#4730,0.18,0.785398163397448);
#231=SHAPE_REPRESENTATION_RELATIONSHIP('SRR','None',#7979,#252);
#252=ADVANCED_BREP_SHAPE_REPRESENTATION('',(#14),#7863);
#281=STYLED_ITEM('',(#8160),#14);
#384=FACE_BOUND('',#1050,.T.);
#499=PLANE('',#4716);
#500=PLANE('',#4724);
#501=PLANE('',#4732);
#502=PLANE('',#4733);
#503=PLANE('',#4734);
#504=PLANE('',#4735);
#505=PLANE('',#4736);
#506=PLANE('',#4737);
#507=PLANE('',#4738);
#508=PLANE('',#4739);
#509=PLANE('',#4740);
#725=FACE_OUTER_BOUND('',#1045,.T.);
#726=FACE_OUTER_BOUND('',#1046,.T.);
#727=FACE_OUTER_BOUND('',#1047,.T.);
#728=FACE_OUTER_BOUND('',#1048,.T.);
#729=FACE_OUTER_BOUND('',#1049,.T.);
#730=FACE_OUTER_BOUND('',#1051,.T.);
#731=FACE_OUTER_BOUND('',#1052,.T.);
#732=FACE_OUTER_BOUND('',#1053,.T.);
#733=FACE_OUTER_BOUND('',#1054,.T.);
#734=FACE_OUTER_BOUND('',#1055,.T.);
#735=FACE_OUTER_BOUND('',#1056,.T.);
#736=FACE_OUTER_BOUND('',#1057,.T.);
#737=FACE_OUTER_BOUND('',#1058,.T.);
#738=FACE_OUTER_BOUND('',#1059,.T.);
#739=FACE_OUTER_BOUND('',#1060,.T.);
#740=FACE_OUTER_BOUND('',#1061,.T.);
#741=FACE_OUTER_BOUND('',#1062,.T.);
#1045=EDGE_LOOP('',(#3431));
#1046=EDGE_LOOP('',(#3432,#3433,#3434,#3435));
#1047=EDGE_LOOP('',(#3436,#3437,#3438,#3439));
#1048=EDGE_LOOP('',(#3440,#3441,#3442,#3443));
#1049=EDGE_LOOP('',(#3444));
#1050=EDGE_LOOP('',(#3445));
#1051=EDGE_LOOP('',(#3446,#3447,#3448,#3449));
#1052=EDGE_LOOP('',(#3450,#3451,#3452,#3453));
#1053=EDGE_LOOP('',(#3454,#3455,#3456,#3457));
#1054=EDGE_LOOP('',(#3458));
#1055=EDGE_LOOP('',(#3459,#3460,#3461,#3462));
#1056=EDGE_LOOP('',(#3463,#3464,#3465,#3466));
#1057=EDGE_LOOP('',(#3467,#3468,#3469,#3470));
#1058=EDGE_LOOP('',(#3471,#3472,#3473,#3474));
#1059=EDGE_LOOP('',(#3475,#3476,#3477,#3478));
#1060=EDGE_LOOP('',(#3479,#3480,#3481,#3482));
#1061=EDGE_LOOP('',(#3483,#3484,#3485,#3486,#3487,#3488));
#1062=EDGE_LOOP('',(#3489,#3490,#3491,#3492,#3493,#3494));
#1301=LINE('',#7326,#1563);
#1302=LINE('',#7330,#1564);
#1303=LINE('',#7334,#1565);
#1304=LINE('',#7341,#1566);
#1305=LINE('',#7345,#1567);
#1306=LINE('',#7349,#1568);
#1307=LINE('',#7354,#1569);
#1308=LINE('',#7356,#1570);
#1309=LINE('',#7358,#1571);
#1310=LINE('',#7359,#1572);
#1311=LINE('',#7362,#1573);
#1312=LINE('',#7364,#1574);
#1313=LINE('',#7365,#1575);
#1314=LINE('',#7368,#1576);
#1315=LINE('',#7370,#1577);
#1316=LINE('',#7371,#1578);
#1317=LINE('',#7374,#1579);
#1318=LINE('',#7376,#1580);
#1319=LINE('',#7377,#1581);
#1320=LINE('',#7380,#1582);
#1321=LINE('',#7382,#1583);
#1322=LINE('',#7383,#1584);
#1323=LINE('',#7385,#1585);
#1324=LINE('',#7386,#1586);
#1563=VECTOR('',#5778,0.325);
#1564=VECTOR('',#5783,0.35);
#1565=VECTOR('',#5788,0.335);
#1566=VECTOR('',#5797,0.21);
#1567=VECTOR('',#5802,0.2);
#1568=VECTOR('',#5807,0.18);
#1569=VECTOR('',#5812,1.);
#1570=VECTOR('',#5813,1.);
#1571=VECTOR('',#5814,1.);
#1572=VECTOR('',#5815,1.);
#1573=VECTOR('',#5818,1.);
#1574=VECTOR('',#5819,1.);
#1575=VECTOR('',#5820,1.);
#1576=VECTOR('',#5823,1.);
#1577=VECTOR('',#5824,1.);
#1578=VECTOR('',#5825,1.);
#1579=VECTOR('',#5828,1.);
#1580=VECTOR('',#5829,1.);
#1581=VECTOR('',#5830,1.);
#1582=VECTOR('',#5833,1.);
#1583=VECTOR('',#5834,1.);
#1584=VECTOR('',#5835,1.);
#1585=VECTOR('',#5838,1.);
#1586=VECTOR('',#5839,1.);
#1843=CIRCLE('',#4717,0.3);
#1844=CIRCLE('',#4719,0.35);
#1845=CIRCLE('',#4721,0.35);
#1846=CIRCLE('',#4723,0.32);
#1847=CIRCLE('',#4725,0.22);
#1848=CIRCLE('',#4727,0.1954);
#1849=CIRCLE('',#4729,0.1954);
#1850=CIRCLE('',#4731,0.16);
#2127=VERTEX_POINT('',#7321);
#2128=VERTEX_POINT('',#7324);
#2129=VERTEX_POINT('',#7328);
#2130=VERTEX_POINT('',#7332);
#2131=VERTEX_POINT('',#7336);
#2132=VERTEX_POINT('',#7339);
#2133=VERTEX_POINT('',#7343);
#2134=VERTEX_POINT('',#7347);
#2135=VERTEX_POINT('',#7352);
#2136=VERTEX_POINT('',#7353);
#2137=VERTEX_POINT('',#7355);
#2138=VERTEX_POINT('',#7357);
#2139=VERTEX_POINT('',#7361);
#2140=VERTEX_POINT('',#7363);
#2141=VERTEX_POINT('',#7367);
#2142=VERTEX_POINT('',#7369);
#2143=VERTEX_POINT('',#7373);
#2144=VERTEX_POINT('',#7375);
#2145=VERTEX_POINT('',#7379);
#2146=VERTEX_POINT('',#7381);
#2579=EDGE_CURVE('',#2127,#2127,#1843,.T.);
#2580=EDGE_CURVE('',#2128,#2128,#1844,.T.);
#2581=EDGE_CURVE('',#2128,#2127,#1301,.T.);
#2582=EDGE_CURVE('',#2129,#2129,#1845,.T.);
#2583=EDGE_CURVE('',#2129,#2128,#1302,.T.);
#2584=EDGE_CURVE('',#2130,#2130,#1846,.T.);
#2585=EDGE_CURVE('',#2130,#2129,#1303,.T.);
#2586=EDGE_CURVE('',#2131,#2131,#1847,.T.);
#2587=EDGE_CURVE('',#2132,#2132,#1848,.F.);
#2588=EDGE_CURVE('',#2132,#2131,#1304,.T.);
#2589=EDGE_CURVE('',#2133,#2133,#1849,.F.);
#2590=EDGE_CURVE('',#2133,#2132,#1305,.T.);
#2591=EDGE_CURVE('',#2134,#2134,#1850,.T.);
#2592=EDGE_CURVE('',#2134,#2133,#1306,.T.);
#2593=EDGE_CURVE('',#2135,#2136,#1307,.T.);
#2594=EDGE_CURVE('',#2136,#2137,#1308,.T.);
#2595=EDGE_CURVE('',#2137,#2138,#1309,.T.);
#2596=EDGE_CURVE('',#2135,#2138,#1310,.T.);
#2597=EDGE_CURVE('',#2136,#2139,#1311,.T.);
#2598=EDGE_CURVE('',#2139,#2140,#1312,.T.);
#2599=EDGE_CURVE('',#2140,#2137,#1313,.T.);
#2600=EDGE_CURVE('',#2139,#2141,#1314,.T.);
#2601=EDGE_CURVE('',#2141,#2142,#1315,.T.);
#2602=EDGE_CURVE('',#2142,#2140,#1316,.T.);
#2603=EDGE_CURVE('',#2141,#2143,#1317,.T.);
#2604=EDGE_CURVE('',#2143,#2144,#1318,.T.);
#2605=EDGE_CURVE('',#2144,#2142,#1319,.T.);
#2606=EDGE_CURVE('',#2143,#2145,#1320,.T.);
#2607=EDGE_CURVE('',#2145,#2146,#1321,.T.);
#2608=EDGE_CURVE('',#2146,#2144,#1322,.T.);
#2609=EDGE_CURVE('',#2145,#2135,#1323,.T.);
#2610=EDGE_CURVE('',#2138,#2146,#1324,.T.);
#3431=ORIENTED_EDGE('',*,*,#2579,.F.);
#3432=ORIENTED_EDGE('',*,*,#2580,.F.);
#3433=ORIENTED_EDGE('',*,*,#2581,.T.);
#3434=ORIENTED_EDGE('',*,*,#2579,.T.);
#3435=ORIENTED_EDGE('',*,*,#2581,.F.);
#3436=ORIENTED_EDGE('',*,*,#2582,.F.);
#3437=ORIENTED_EDGE('',*,*,#2583,.T.);
#3438=ORIENTED_EDGE('',*,*,#2580,.T.);
#3439=ORIENTED_EDGE('',*,*,#2583,.F.);
#3440=ORIENTED_EDGE('',*,*,#2584,.F.);
#3441=ORIENTED_EDGE('',*,*,#2585,.T.);
#3442=ORIENTED_EDGE('',*,*,#2582,.T.);
#3443=ORIENTED_EDGE('',*,*,#2585,.F.);
#3444=ORIENTED_EDGE('',*,*,#2584,.T.);
#3445=ORIENTED_EDGE('',*,*,#2586,.F.);
#3446=ORIENTED_EDGE('',*,*,#2587,.F.);
#3447=ORIENTED_EDGE('',*,*,#2588,.T.);
#3448=ORIENTED_EDGE('',*,*,#2586,.T.);
#3449=ORIENTED_EDGE('',*,*,#2588,.F.);
#3450=ORIENTED_EDGE('',*,*,#2589,.F.);
#3451=ORIENTED_EDGE('',*,*,#2590,.T.);
#3452=ORIENTED_EDGE('',*,*,#2587,.T.);
#3453=ORIENTED_EDGE('',*,*,#2590,.F.);
#3454=ORIENTED_EDGE('',*,*,#2591,.F.);
#3455=ORIENTED_EDGE('',*,*,#2592,.T.);
#3456=ORIENTED_EDGE('',*,*,#2589,.T.);
#3457=ORIENTED_EDGE('',*,*,#2592,.F.);
#3458=ORIENTED_EDGE('',*,*,#2591,.T.);
#3459=ORIENTED_EDGE('',*,*,#2593,.T.);
#3460=ORIENTED_EDGE('',*,*,#2594,.T.);
#3461=ORIENTED_EDGE('',*,*,#2595,.T.);
#3462=ORIENTED_EDGE('',*,*,#2596,.F.);
#3463=ORIENTED_EDGE('',*,*,#2597,.T.);
#3464=ORIENTED_EDGE('',*,*,#2598,.T.);
#3465=ORIENTED_EDGE('',*,*,#2599,.T.);
#3466=ORIENTED_EDGE('',*,*,#2594,.F.);
#3467=ORIENTED_EDGE('',*,*,#2600,.T.);
#3468=ORIENTED_EDGE('',*,*,#2601,.T.);
#3469=ORIENTED_EDGE('',*,*,#2602,.T.);
#3470=ORIENTED_EDGE('',*,*,#2598,.F.);
#3471=ORIENTED_EDGE('',*,*,#2603,.T.);
#3472=ORIENTED_EDGE('',*,*,#2604,.T.);
#3473=ORIENTED_EDGE('',*,*,#2605,.T.);
#3474=ORIENTED_EDGE('',*,*,#2601,.F.);
#3475=ORIENTED_EDGE('',*,*,#2606,.T.);
#3476=ORIENTED_EDGE('',*,*,#2607,.T.);
#3477=ORIENTED_EDGE('',*,*,#2608,.T.);
#3478=ORIENTED_EDGE('',*,*,#2604,.F.);
#3479=ORIENTED_EDGE('',*,*,#2609,.T.);
#3480=ORIENTED_EDGE('',*,*,#2596,.T.);
#3481=ORIENTED_EDGE('',*,*,#2610,.T.);
#3482=ORIENTED_EDGE('',*,*,#2607,.F.);
#3483=ORIENTED_EDGE('',*,*,#2609,.F.);
#3484=ORIENTED_EDGE('',*,*,#2606,.F.);
#3485=ORIENTED_EDGE('',*,*,#2603,.F.);
#3486=ORIENTED_EDGE('',*,*,#2600,.F.);
#3487=ORIENTED_EDGE('',*,*,#2597,.F.);
#3488=ORIENTED_EDGE('',*,*,#2593,.F.);
#3489=ORIENTED_EDGE('',*,*,#2610,.F.);
#3490=ORIENTED_EDGE('',*,*,#2595,.F.);
#3491=ORIENTED_EDGE('',*,*,#2599,.F.);
#3492=ORIENTED_EDGE('',*,*,#2602,.F.);
#3493=ORIENTED_EDGE('',*,*,#2605,.F.);
#3494=ORIENTED_EDGE('',*,*,#2608,.F.);
#3815=CYLINDRICAL_SURFACE('',#4720,0.35);
#3816=CYLINDRICAL_SURFACE('',#4728,0.1954);
#4007=ADVANCED_FACE('',(#725),#499,.T.);
#4008=ADVANCED_FACE('',(#726),#209,.T.);
#4009=ADVANCED_FACE('',(#727),#3815,.T.);
#4010=ADVANCED_FACE('',(#728),#210,.T.);
#4011=ADVANCED_FACE('',(#729,#384),#500,.T.);
#4012=ADVANCED_FACE('',(#730),#211,.T.);
#4013=ADVANCED_FACE('',(#731),#3816,.T.);
#4014=ADVANCED_FACE('',(#732),#212,.T.);
#4015=ADVANCED_FACE('',(#733),#501,.T.);
#4016=ADVANCED_FACE('',(#734),#502,.F.);
#4017=ADVANCED_FACE('',(#735),#503,.F.);
#4018=ADVANCED_FACE('',(#736),#504,.F.);
#4019=ADVANCED_FACE('',(#737),#505,.F.);
#4020=ADVANCED_FACE('',(#738),#506,.F.);
#4021=ADVANCED_FACE('',(#739),#507,.F.);
#4022=ADVANCED_FACE('',(#740),#508,.F.);
#4023=ADVANCED_FACE('',(#741),#509,.F.);
#4108=CLOSED_SHELL('',(#4007,#4008,#4009,#4010,#4011,#4012,#4013,#4014,
#4015));
#4109=CLOSED_SHELL('',(#4016,#4017,#4018,#4019,#4020,#4021,#4022,#4023));
#4715=AXIS2_PLACEMENT_3D('',#7319,#5768,#5769);
#4716=AXIS2_PLACEMENT_3D('',#7320,#5770,#5771);
#4717=AXIS2_PLACEMENT_3D('',#7322,#5772,#5773);
#4718=AXIS2_PLACEMENT_3D('',#7323,#5774,#5775);
#4719=AXIS2_PLACEMENT_3D('',#7325,#5776,#5777);
#4720=AXIS2_PLACEMENT_3D('',#7327,#5779,#5780);
#4721=AXIS2_PLACEMENT_3D('',#7329,#5781,#5782);
#4722=AXIS2_PLACEMENT_3D('',#7331,#5784,#5785);
#4723=AXIS2_PLACEMENT_3D('',#7333,#5786,#5787);
#4724=AXIS2_PLACEMENT_3D('',#7335,#5789,#5790);
#4725=AXIS2_PLACEMENT_3D('',#7337,#5791,#5792);
#4726=AXIS2_PLACEMENT_3D('',#7338,#5793,#5794);
#4727=AXIS2_PLACEMENT_3D('',#7340,#5795,#5796);
#4728=AXIS2_PLACEMENT_3D('',#7342,#5798,#5799);
#4729=AXIS2_PLACEMENT_3D('',#7344,#5800,#5801);
#4730=AXIS2_PLACEMENT_3D('',#7346,#5803,#5804);
#4731=AXIS2_PLACEMENT_3D('',#7348,#5805,#5806);
#4732=AXIS2_PLACEMENT_3D('',#7350,#5808,#5809);
#4733=AXIS2_PLACEMENT_3D('',#7351,#5810,#5811);
#4734=AXIS2_PLACEMENT_3D('',#7360,#5816,#5817);
#4735=AXIS2_PLACEMENT_3D('',#7366,#5821,#5822);
#4736=AXIS2_PLACEMENT_3D('',#7372,#5826,#5827);
#4737=AXIS2_PLACEMENT_3D('',#7378,#5831,#5832);
#4738=AXIS2_PLACEMENT_3D('',#7384,#5836,#5837);
#4739=AXIS2_PLACEMENT_3D('',#7387,#5840,#5841);
#4740=AXIS2_PLACEMENT_3D('',#7388,#5842,#5843);
#5768=DIRECTION('axis',(0.,0.,1.));
#5769=DIRECTION('refdir',(1.,0.,0.));
#5770=DIRECTION('center_axis',(0.,1.,0.));
#5771=DIRECTION('ref_axis',(0.,0.,1.));
#5772=DIRECTION('center_axis',(0.,-1.,0.));
#5773=DIRECTION('ref_axis',(1.,0.,0.));
#5774=DIRECTION('center_axis',(0.,-1.,0.));
#5775=DIRECTION('ref_axis',(1.,0.,0.));
#5776=DIRECTION('center_axis',(0.,-1.,0.));
#5777=DIRECTION('ref_axis',(1.,0.,0.));
#5778=DIRECTION('',(0.707106781186547,0.707106781186548,8.65956056235493E-17));
#5779=DIRECTION('center_axis',(0.,-1.,0.));
#5780=DIRECTION('ref_axis',(1.,0.,0.));
#5781=DIRECTION('center_axis',(0.,-1.,0.));
#5782=DIRECTION('ref_axis',(1.,0.,0.));
#5783=DIRECTION('',(0.,1.,0.));
#5784=DIRECTION('center_axis',(0.,1.,0.));
#5785=DIRECTION('ref_axis',(1.,0.,0.));
#5786=DIRECTION('center_axis',(0.,-1.,0.));
#5787=DIRECTION('ref_axis',(1.,0.,0.));
#5788=DIRECTION('',(-0.707106781186547,0.707106781186548,-8.65956056235493E-17));
#5789=DIRECTION('center_axis',(0.,-1.,0.));
#5790=DIRECTION('ref_axis',(0.,0.,-1.));
#5791=DIRECTION('center_axis',(0.,-1.,0.));
#5792=DIRECTION('ref_axis',(1.,0.,0.));
#5793=DIRECTION('center_axis',(0.,1.,0.));
#5794=DIRECTION('ref_axis',(1.,0.,0.));
#5795=DIRECTION('center_axis',(0.,1.,0.));
#5796=DIRECTION('ref_axis',(1.,0.,0.));
#5797=DIRECTION('',(-0.447213595499958,0.894427190999916,-5.47678698264203E-17));
#5798=DIRECTION('center_axis',(0.,-1.,0.));
#5799=DIRECTION('ref_axis',(1.,0.,0.));
#5800=DIRECTION('center_axis',(0.,1.,0.));
#5801=DIRECTION('ref_axis',(1.,0.,0.));
#5802=DIRECTION('',(0.,1.,0.));
#5803=DIRECTION('center_axis',(0.,1.,0.));
#5804=DIRECTION('ref_axis',(1.,0.,0.));
#5805=DIRECTION('center_axis',(0.,-1.,0.));
#5806=DIRECTION('ref_axis',(1.,0.,0.));
#5807=DIRECTION('',(-0.707106781186547,0.707106781186548,-8.65956056235493E-17));
#5808=DIRECTION('center_axis',(0.,-1.,0.));
#5809=DIRECTION('ref_axis',(0.,0.,-1.));
#5810=DIRECTION('center_axis',(0.866025403784439,0.,-0.5));
#5811=DIRECTION('ref_axis',(0.5,0.,0.866025403784439));
#5812=DIRECTION('',(-0.5,0.,-0.866025403784439));
#5813=DIRECTION('',(0.,-1.,0.));
#5814=DIRECTION('',(0.5,0.,0.866025403784439));
#5815=DIRECTION('',(0.,-1.,0.));
#5816=DIRECTION('center_axis',(1.60246890531964E-16,0.,-1.));
#5817=DIRECTION('ref_axis',(1.,0.,1.60246890531964E-16));
#5818=DIRECTION('',(-1.,0.,-1.60246890531964E-16));
#5819=DIRECTION('',(0.,-1.,0.));
#5820=DIRECTION('',(1.,0.,1.60246890531964E-16));
#5821=DIRECTION('center_axis',(-0.866025403784439,0.,-0.5));
#5822=DIRECTION('ref_axis',(0.5,0.,-0.866025403784439));
#5823=DIRECTION('',(-0.5,0.,0.866025403784439));
#5824=DIRECTION('',(0.,-1.,0.));
#5825=DIRECTION('',(0.5,0.,-0.866025403784439));
#5826=DIRECTION('center_axis',(-0.866025403784439,0.,0.5));
#5827=DIRECTION('ref_axis',(-0.5,0.,-0.866025403784439));
#5828=DIRECTION('',(0.5,0.,0.866025403784439));
#5829=DIRECTION('',(0.,-1.,0.));
#5830=DIRECTION('',(-0.5,0.,-0.866025403784439));
#5831=DIRECTION('center_axis',(-1.60246890531964E-16,0.,1.));
#5832=DIRECTION('ref_axis',(-1.,0.,-1.60246890531964E-16));
#5833=DIRECTION('',(1.,0.,1.60246890531964E-16));
#5834=DIRECTION('',(0.,-1.,0.));
#5835=DIRECTION('',(-1.,0.,-1.60246890531964E-16));
#5836=DIRECTION('center_axis',(0.866025403784439,0.,0.5));
#5837=DIRECTION('ref_axis',(-0.5,0.,0.866025403784439));
#5838=DIRECTION('',(0.5,0.,-0.866025403784439));
#5839=DIRECTION('',(-0.5,0.,0.866025403784439));
#5840=DIRECTION('center_axis',(0.,1.,0.));
#5841=DIRECTION('ref_axis',(1.,0.,0.));
#5842=DIRECTION('center_axis',(0.,-1.,0.));
#5843=DIRECTION('ref_axis',(0.,0.,-1.));
#7319=CARTESIAN_POINT('',(0.,0.,0.));
#7320=CARTESIAN_POINT('Origin',(0.3,0.4,0.));
#7321=CARTESIAN_POINT('',(-0.3,0.4,-3.67394039744206E-17));
#7322=CARTESIAN_POINT('Origin',(0.,0.4,0.));
#7323=CARTESIAN_POINT('Origin',(0.,0.375,0.));
#7324=CARTESIAN_POINT('',(-0.35,0.35,-4.28626379701573E-17));
#7325=CARTESIAN_POINT('Origin',(0.,0.35,0.));
#7326=CARTESIAN_POINT('',(-0.325,0.375,-3.9801020972289E-17));
#7327=CARTESIAN_POINT('Origin',(0.,0.19,0.));
#7328=CARTESIAN_POINT('',(-0.35,0.03,-4.28626379701574E-17));
#7329=CARTESIAN_POINT('Origin',(0.,0.03,0.));
#7330=CARTESIAN_POINT('',(-0.35,0.19,-4.28626379701574E-17));
#7331=CARTESIAN_POINT('Origin',(0.,0.0149999999999999,0.));
#7332=CARTESIAN_POINT('',(-0.32,-3.29597460435593E-17,-3.91886975727153E-17));
#7333=CARTESIAN_POINT('Origin',(0.,0.,0.));
#7334=CARTESIAN_POINT('',(-0.335,0.0149999999999999,-4.10256677714363E-17));
#7335=CARTESIAN_POINT('Origin',(0.22,0.,0.));
#7336=CARTESIAN_POINT('',(-0.22,-6.93889390390723E-18,-2.69422295812418E-17));
#7337=CARTESIAN_POINT('Origin',(0.,0.,0.));
#7338=CARTESIAN_POINT('Origin',(0.,-0.02,0.));
#7339=CARTESIAN_POINT('',(-0.1954,-0.0492,2.39295984553393E-17));
#7340=CARTESIAN_POINT('Origin',(0.,-0.0492,0.));
#7341=CARTESIAN_POINT('',(-0.21,-0.02,-2.57175827820944E-17));
#7342=CARTESIAN_POINT('Origin',(0.,-0.8,0.));
#7343=CARTESIAN_POINT('',(-0.1954,-1.5646,2.39295984553393E-17));
#7344=CARTESIAN_POINT('Origin',(0.,-1.5646,0.));
#7345=CARTESIAN_POINT('',(-0.1954,-0.8,-2.39295984553393E-17));
#7346=CARTESIAN_POINT('Origin',(0.,-1.58,0.));
#7347=CARTESIAN_POINT('',(-0.16,-1.6,-1.95943487863577E-17));
#7348=CARTESIAN_POINT('Origin',(0.,-1.6,0.));
#7349=CARTESIAN_POINT('',(-0.18,-1.58,-2.20436423846524E-17));
#7350=CARTESIAN_POINT('Origin',(0.,-1.6,0.));
#7351=CARTESIAN_POINT('Origin',(0.0866025403784439,-0.4,-0.15));
#7352=CARTESIAN_POINT('',(0.173205080756888,-0.4,0.));
#7353=CARTESIAN_POINT('',(0.0866025403784439,-0.4,-0.15));
#7354=CARTESIAN_POINT('',(0.173205080756888,-0.4,0.));
#7355=CARTESIAN_POINT('',(0.0866025403784439,-0.64,-0.15));
#7356=CARTESIAN_POINT('',(0.0866025403784439,-0.4,-0.15));
#7357=CARTESIAN_POINT('',(0.173205080756888,-0.64,0.));
#7358=CARTESIAN_POINT('',(0.173205080756888,-0.64,0.));
#7359=CARTESIAN_POINT('',(0.173205080756888,-0.4,0.));
#7360=CARTESIAN_POINT('Origin',(-0.0866025403784438,-0.4,-0.15));
#7361=CARTESIAN_POINT('',(-0.0866025403784438,-0.4,-0.15));
#7362=CARTESIAN_POINT('',(0.0866025403784439,-0.4,-0.15));
#7363=CARTESIAN_POINT('',(-0.0866025403784438,-0.64,-0.15));
#7364=CARTESIAN_POINT('',(-0.0866025403784438,-0.4,-0.15));
#7365=CARTESIAN_POINT('',(0.0866025403784439,-0.64,-0.15));
#7366=CARTESIAN_POINT('Origin',(-0.173205080756888,-0.4,-2.77555756156289E-17));
#7367=CARTESIAN_POINT('',(-0.173205080756888,-0.4,-2.12115047744981E-17));
#7368=CARTESIAN_POINT('',(-0.0866025403784438,-0.4,-0.15));
#7369=CARTESIAN_POINT('',(-0.173205080756888,-0.64,-2.77555756156289E-17));
#7370=CARTESIAN_POINT('',(-0.173205080756888,-0.4,-2.12115047744981E-17));
#7371=CARTESIAN_POINT('',(-0.0866025403784438,-0.64,-0.15));
#7372=CARTESIAN_POINT('Origin',(-0.0866025403784439,-0.4,0.15));
#7373=CARTESIAN_POINT('',(-0.0866025403784439,-0.4,0.15));
#7374=CARTESIAN_POINT('',(-0.173205080756888,-0.4,-2.12115047744981E-17));
#7375=CARTESIAN_POINT('',(-0.0866025403784439,-0.64,0.15));
#7376=CARTESIAN_POINT('',(-0.0866025403784439,-0.4,0.15));
#7377=CARTESIAN_POINT('',(-0.173205080756888,-0.64,-2.12115047744981E-17));
#7378=CARTESIAN_POINT('Origin',(0.0866025403784439,-0.4,0.15));
#7379=CARTESIAN_POINT('',(0.0866025403784439,-0.4,0.15));
#7380=CARTESIAN_POINT('',(-0.0866025403784439,-0.4,0.15));
#7381=CARTESIAN_POINT('',(0.0866025403784439,-0.64,0.15));
#7382=CARTESIAN_POINT('',(0.0866025403784439,-0.4,0.15));
#7383=CARTESIAN_POINT('',(-0.0866025403784439,-0.64,0.15));
#7384=CARTESIAN_POINT('Origin',(0.173205080756888,-0.4,0.));
#7385=CARTESIAN_POINT('',(0.0866025403784439,-0.4,0.15));
#7386=CARTESIAN_POINT('',(0.0866025403784439,-0.64,0.15));
#7387=CARTESIAN_POINT('Origin',(0.,-0.4,-2.77555756156289E-17));
#7388=CARTESIAN_POINT('Origin',(0.,-0.64,-2.77555756156289E-17));
#7837=UNCERTAINTY_MEASURE_WITH_UNIT(LENGTH_MEASURE(0.001),#7872,
'DISTANCE_ACCURACY_VALUE',
'Maximum model space distance between geometric entities at asserted c
onnectivities');
#7845=UNCERTAINTY_MEASURE_WITH_UNIT(LENGTH_MEASURE(0.001),#7872,
'DISTANCE_ACCURACY_VALUE',
'Maximum model space distance between geometric entities at asserted c
onnectivities');
#7863=(
GEOMETRIC_REPRESENTATION_CONTEXT(3)
GLOBAL_UNCERTAINTY_ASSIGNED_CONTEXT((#7837))
GLOBAL_UNIT_ASSIGNED_CONTEXT((#7872,#7874,#7875))
REPRESENTATION_CONTEXT('','3D')
);
#7871=(
GEOMETRIC_REPRESENTATION_CONTEXT(3)
GLOBAL_UNCERTAINTY_ASSIGNED_CONTEXT((#7845))
GLOBAL_UNIT_ASSIGNED_CONTEXT((#7872,#7874,#7875))
REPRESENTATION_CONTEXT('','3D')
);
#7872=(
LENGTH_UNIT()
NAMED_UNIT(*)
SI_UNIT(.CENTI.,.METRE.)
);
#7874=(
NAMED_UNIT(*)
PLANE_ANGLE_UNIT()
SI_UNIT($,.RADIAN.)
);
#7875=(
NAMED_UNIT(*)
SI_UNIT($,.STERADIAN.)
SOLID_ANGLE_UNIT()
);
#7893=SHAPE_DEFINITION_REPRESENTATION(#7923,#7979);
#7923=PRODUCT_DEFINITION_SHAPE('',$,#8005);
#7979=SHAPE_REPRESENTATION('',(#4715),#7863);
#7987=PRODUCT_DEFINITION_CONTEXT('part definition',#8064,'design');
#8005=PRODUCT_DEFINITION('Cap Screw - M4x16','Cap Screw - M4x16',#8030,
#7987);
#8030=PRODUCT_DEFINITION_FORMATION('',$,#8083);
#8064=APPLICATION_CONTEXT(
'Core Data for Automotive Mechanical Design Process');
#8065=PRODUCT_CONTEXT('part definition',#8064,'mechanical');
#8083=PRODUCT('Cap Screw - M4x16','Cap Screw - M4x16',
'Cap Screw - M4x16',(#8065));
#8154=COLOUR_RGB('Black',0.12,0.14,0.17);
#8155=FILL_AREA_STYLE_COLOUR('',#8154);
#8156=FILL_AREA_STYLE('',(#8155));
#8157=SURFACE_STYLE_FILL_AREA(#8156);
#8158=SURFACE_SIDE_STYLE('',(#8157));
#8159=SURFACE_STYLE_USAGE(.BOTH.,#8158);
#8160=PRESENTATION_STYLE_ASSIGNMENT((#8159));
ENDSEC;
END-ISO-10303-21;
